ISO-10303-21;
HEADER;
/* Generated by software containing ST-Developer
 * from STEP Tools, Inc. (www.steptools.com) 
 */

FILE_DESCRIPTION(
/* description */ ('Spring compression tester'),
/* implementation_level */ '2;1');

FILE_NAME(
/* name */ 'Nut carrier.step',
/* time_stamp */ '2026-10-28T03:24:11-07:00',
/* author */ (''),
/* organization */ (''),
/* preprocessor_version */ 'ST-DEVELOPER v20.2',
/* originating_system */ 'Autodesk Translation Framework v15.17.0.0',
/* authorisation */ '');

FILE_SCHEMA (('AUTOMOTIVE_DESIGN { 1 0 10303 214 3 1 1 }'));
ENDSEC;

DATA;
#10=MECHANICAL_DESIGN_GEOMETRIC_PRESENTATION_REPRESENTATION('',(#1161),#43521);
#1026=SHAPE_REPRESENTATION_RELATIONSHIP('SRR','None',#43841,#1086);
#1086=ADVANCED_BREP_SHAPE_REPRESENTATION('',(#1232),#43501);
#1161=STYLED_ITEM('',(#44209),#1232);
#1232=MANIFOLD_SOLID_BREP('Body1',#18602);
#1529=FACE_BOUND('',#4216,.T.);
#1530=FACE_BOUND('',#4217,.T.);
#1531=FACE_BOUND('',#4218,.T.);
#1532=FACE_BOUND('',#4219,.T.);
#1533=FACE_BOUND('',#4221,.T.);
#2046=PLANE('',#20590);
#2047=PLANE('',#20594);
#2048=PLANE('',#20598);
#2049=PLANE('',#20605);
#2050=PLANE('',#20606);
#2878=FACE_OUTER_BOUND('',#4207,.T.);
#2879=FACE_OUTER_BOUND('',#4208,.T.);
#2880=FACE_OUTER_BOUND('',#4209,.T.);
#2881=FACE_OUTER_BOUND('',#4210,.T.);
#2882=FACE_OUTER_BOUND('',#4211,.T.);
#2883=FACE_OUTER_BOUND('',#4212,.T.);
#2884=FACE_OUTER_BOUND('',#4213,.T.);
#2885=FACE_OUTER_BOUND('',#4214,.T.);
#2886=FACE_OUTER_BOUND('',#4215,.T.);
#2887=FACE_OUTER_BOUND('',#4220,.T.);
#4207=EDGE_LOOP('',(#15453,#15454,#15455,#15456));
#4208=EDGE_LOOP('',(#15457));
#4209=EDGE_LOOP('',(#15458,#15459,#15460,#15461));
#4210=EDGE_LOOP('',(#15462));
#4211=EDGE_LOOP('',(#15463,#15464,#15465,#15466));
#4212=EDGE_LOOP('',(#15467));
#4213=EDGE_LOOP('',(#15468,#15469,#15470,#15471));
#4214=EDGE_LOOP('',(#15472,#15473,#15474,#15475));
#4215=EDGE_LOOP('',(#15476));
#4216=EDGE_LOOP('',(#15477));
#4217=EDGE_LOOP('',(#15478));
#4218=EDGE_LOOP('',(#15479));
#4219=EDGE_LOOP('',(#15480));
#4220=EDGE_LOOP('',(#15481));
#4221=EDGE_LOOP('',(#15482));
#5655=LINE('',#30562,#7087);
#5656=LINE('',#30569,#7088);
#5657=LINE('',#30576,#7089);
#5658=LINE('',#30583,#7090);
#5659=LINE('',#30589,#7091);
#7087=VECTOR('',#24855,0.165);
#7088=VECTOR('',#24864,0.165);
#7089=VECTOR('',#24873,0.165);
#7090=VECTOR('',#24882,1.11);
#7091=VECTOR('',#24889,2.2);
#8005=CIRCLE('',#20588,0.165);
#8006=CIRCLE('',#20589,0.165);
#8007=CIRCLE('',#20592,0.165);
#8008=CIRCLE('',#20593,0.165);
#8009=CIRCLE('',#20596,0.165);
#8010=CIRCLE('',#20597,0.165);
#8011=CIRCLE('',#20600,1.11);
#8012=CIRCLE('',#20601,1.11);
#8013=CIRCLE('',#20603,2.2);
#8014=CIRCLE('',#20604,2.2);
#9226=VERTEX_POINT('',#30559);
#9227=VERTEX_POINT('',#30561);
#9228=VERTEX_POINT('',#30566);
#9229=VERTEX_POINT('',#30568);
#9230=VERTEX_POINT('',#30573);
#9231=VERTEX_POINT('',#30575);
#9232=VERTEX_POINT('',#30580);
#9233=VERTEX_POINT('',#30582);
#9234=VERTEX_POINT('',#30586);
#9235=VERTEX_POINT('',#30588);
#11391=EDGE_CURVE('',#9226,#9226,#8005,.T.);
#11392=EDGE_CURVE('',#9226,#9227,#5655,.T.);
#11393=EDGE_CURVE('',#9227,#9227,#8006,.T.);
#11394=EDGE_CURVE('',#9228,#9228,#8007,.T.);
#11395=EDGE_CURVE('',#9228,#9229,#5656,.T.);
#11396=EDGE_CURVE('',#9229,#9229,#8008,.T.);
#11397=EDGE_CURVE('',#9230,#9230,#8009,.T.);
#11398=EDGE_CURVE('',#9230,#9231,#5657,.T.);
#11399=EDGE_CURVE('',#9231,#9231,#8010,.T.);
#11400=EDGE_CURVE('',#9232,#9232,#8011,.T.);
#11401=EDGE_CURVE('',#9232,#9233,#5658,.T.);
#11402=EDGE_CURVE('',#9233,#9233,#8012,.T.);
#11403=EDGE_CURVE('',#9234,#9234,#8013,.T.);
#11404=EDGE_CURVE('',#9234,#9235,#5659,.T.);
#11405=EDGE_CURVE('',#9235,#9235,#8014,.T.);
#15453=ORIENTED_EDGE('',*,*,#11391,.F.);
#15454=ORIENTED_EDGE('',*,*,#11392,.T.);
#15455=ORIENTED_EDGE('',*,*,#11393,.F.);
#15456=ORIENTED_EDGE('',*,*,#11392,.F.);
#15457=ORIENTED_EDGE('',*,*,#11391,.T.);
#15458=ORIENTED_EDGE('',*,*,#11394,.F.);
#15459=ORIENTED_EDGE('',*,*,#11395,.T.);
#15460=ORIENTED_EDGE('',*,*,#11396,.F.);
#15461=ORIENTED_EDGE('',*,*,#11395,.F.);
#15462=ORIENTED_EDGE('',*,*,#11394,.T.);
#15463=ORIENTED_EDGE('',*,*,#11397,.F.);
#15464=ORIENTED_EDGE('',*,*,#11398,.T.);
#15465=ORIENTED_EDGE('',*,*,#11399,.F.);
#15466=ORIENTED_EDGE('',*,*,#11398,.F.);
#15467=ORIENTED_EDGE('',*,*,#11397,.T.);
#15468=ORIENTED_EDGE('',*,*,#11400,.F.);
#15469=ORIENTED_EDGE('',*,*,#11401,.T.);
#15470=ORIENTED_EDGE('',*,*,#11402,.T.);
#15471=ORIENTED_EDGE('',*,*,#11401,.F.);
#15472=ORIENTED_EDGE('',*,*,#11403,.F.);
#15473=ORIENTED_EDGE('',*,*,#11404,.T.);
#15474=ORIENTED_EDGE('',*,*,#11405,.T.);
#15475=ORIENTED_EDGE('',*,*,#11404,.F.);
#15476=ORIENTED_EDGE('',*,*,#11403,.T.);
#15477=ORIENTED_EDGE('',*,*,#11393,.T.);
#15478=ORIENTED_EDGE('',*,*,#11396,.T.);
#15479=ORIENTED_EDGE('',*,*,#11399,.T.);
#15480=ORIENTED_EDGE('',*,*,#11400,.T.);
#15481=ORIENTED_EDGE('',*,*,#11405,.F.);
#15482=ORIENTED_EDGE('',*,*,#11402,.F.);
#17296=CYLINDRICAL_SURFACE('',#20587,0.165);
#17297=CYLINDRICAL_SURFACE('',#20591,0.165);
#17298=CYLINDRICAL_SURFACE('',#20595,0.165);
#17299=CYLINDRICAL_SURFACE('',#20599,1.11);
#17300=CYLINDRICAL_SURFACE('',#20602,2.2);
#18202=ADVANCED_FACE('',(#2878),#17296,.F.);
#18203=ADVANCED_FACE('',(#2879),#2046,.T.);
#18204=ADVANCED_FACE('',(#2880),#17297,.F.);
#18205=ADVANCED_FACE('',(#2881),#2047,.T.);
#18206=ADVANCED_FACE('',(#2882),#17298,.F.);
#18207=ADVANCED_FACE('',(#2883),#2048,.T.);
#18208=ADVANCED_FACE('',(#2884),#17299,.F.);
#18209=ADVANCED_FACE('',(#2885),#17300,.T.);
#18210=ADVANCED_FACE('',(#2886,#1529,#1530,#1531,#1532),#2049,.T.);
#18211=ADVANCED_FACE('',(#2887,#1533),#2050,.F.);
#18602=CLOSED_SHELL('',(#18202,#18203,#18204,#18205,#18206,#18207,#18208,
#18209,#18210,#18211));
#20586=AXIS2_PLACEMENT_3D('',#30557,#24849,#24850);
#20587=AXIS2_PLACEMENT_3D('',#30558,#24851,#24852);
#20588=AXIS2_PLACEMENT_3D('',#30560,#24853,#24854);
#20589=AXIS2_PLACEMENT_3D('',#30563,#24856,#24857);
#20590=AXIS2_PLACEMENT_3D('',#30564,#24858,#24859);
#20591=AXIS2_PLACEMENT_3D('',#30565,#24860,#24861);
#20592=AXIS2_PLACEMENT_3D('',#30567,#24862,#24863);
#20593=AXIS2_PLACEMENT_3D('',#30570,#24865,#24866);
#20594=AXIS2_PLACEMENT_3D('',#30571,#24867,#24868);
#20595=AXIS2_PLACEMENT_3D('',#30572,#24869,#24870);
#20596=AXIS2_PLACEMENT_3D('',#30574,#24871,#24872);
#20597=AXIS2_PLACEMENT_3D('',#30577,#24874,#24875);
#20598=AXIS2_PLACEMENT_3D('',#30578,#24876,#24877);
#20599=AXIS2_PLACEMENT_3D('',#30579,#24878,#24879);
#20600=AXIS2_PLACEMENT_3D('',#30581,#24880,#24881);
#20601=AXIS2_PLACEMENT_3D('',#30584,#24883,#24884);
#20602=AXIS2_PLACEMENT_3D('',#30585,#24885,#24886);
#20603=AXIS2_PLACEMENT_3D('',#30587,#24887,#24888);
#20604=AXIS2_PLACEMENT_3D('',#30590,#24890,#24891);
#20605=AXIS2_PLACEMENT_3D('',#30591,#24892,#24893);
#20606=AXIS2_PLACEMENT_3D('',#30592,#24894,#24895);
#24849=DIRECTION('axis',(0.,0.,1.));
#24850=DIRECTION('refdir',(1.,0.,0.));
#24851=DIRECTION('center_axis',(0.,0.,1.));
#24852=DIRECTION('ref_axis',(1.,0.,0.));
#24853=DIRECTION('center_axis',(0.,0.,1.));
#24854=DIRECTION('ref_axis',(1.,0.,0.));
#24855=DIRECTION('',(0.,0.,1.));
#24856=DIRECTION('center_axis',(0.,0.,-1.));
#24857=DIRECTION('ref_axis',(1.,0.,0.));
#24858=DIRECTION('center_axis',(0.,0.,1.));
#24859=DIRECTION('ref_axis',(1.,0.,0.));
#24860=DIRECTION('center_axis',(0.,0.,1.));
#24861=DIRECTION('ref_axis',(1.,0.,0.));
#24862=DIRECTION('center_axis',(0.,0.,1.));
#24863=DIRECTION('ref_axis',(1.,0.,0.));
#24864=DIRECTION('',(0.,0.,1.));
#24865=DIRECTION('center_axis',(0.,0.,-1.));
#24866=DIRECTION('ref_axis',(1.,0.,0.));
#24867=DIRECTION('center_axis',(0.,0.,1.));
#24868=DIRECTION('ref_axis',(1.,0.,0.));
#24869=DIRECTION('center_axis',(0.,0.,1.));
#24870=DIRECTION('ref_axis',(1.,0.,0.));
#24871=DIRECTION('center_axis',(0.,0.,1.));
#24872=DIRECTION('ref_axis',(1.,0.,0.));
#24873=DIRECTION('',(0.,0.,1.));
#24874=DIRECTION('center_axis',(0.,0.,-1.));
#24875=DIRECTION('ref_axis',(1.,0.,0.));
#24876=DIRECTION('center_axis',(0.,0.,1.));
#24877=DIRECTION('ref_axis',(1.,0.,0.));
#24878=DIRECTION('center_axis',(0.,0.,1.));
#24879=DIRECTION('ref_axis',(1.,0.,0.));
#24880=DIRECTION('center_axis',(0.,0.,-1.));
#24881=DIRECTION('ref_axis',(1.,0.,0.));
#24882=DIRECTION('',(0.,0.,-1.));
#24883=DIRECTION('center_axis',(0.,0.,-1.));
#24884=DIRECTION('ref_axis',(1.,0.,0.));
#24885=DIRECTION('center_axis',(0.,0.,1.));
#24886=DIRECTION('ref_axis',(1.,0.,0.));
#24887=DIRECTION('center_axis',(0.,0.,1.));
#24888=DIRECTION('ref_axis',(1.,0.,0.));
#24889=DIRECTION('',(0.,0.,-1.));
#24890=DIRECTION('center_axis',(0.,0.,1.));
#24891=DIRECTION('ref_axis',(1.,0.,0.));
#24892=DIRECTION('center_axis',(0.,0.,1.));
#24893=DIRECTION('ref_axis',(1.,0.,0.));
#24894=DIRECTION('center_axis',(0.,0.,1.));
#24895=DIRECTION('ref_axis',(1.,0.,0.));
#30557=CARTESIAN_POINT('',(0.,0.,0.));
#30558=CARTESIAN_POINT('Origin',(0.,3.5,12.8));
#30559=CARTESIAN_POINT('',(-0.165,3.5,12.8));
#30560=CARTESIAN_POINT('Origin',(0.,3.5,12.8));
#30561=CARTESIAN_POINT('',(-0.165,3.5,14.5));
#30562=CARTESIAN_POINT('',(-0.165,3.5,12.8));
#30563=CARTESIAN_POINT('Origin',(0.,3.5,14.5));
#30564=CARTESIAN_POINT('Origin',(0.,3.5,12.8));
#30565=CARTESIAN_POINT('Origin',(0.,6.5,12.8));
#30566=CARTESIAN_POINT('',(-0.165,6.5,12.8));
#30567=CARTESIAN_POINT('Origin',(0.,6.5,12.8));
#30568=CARTESIAN_POINT('',(-0.165,6.5,14.5));
#30569=CARTESIAN_POINT('',(-0.165,6.5,12.8));
#30570=CARTESIAN_POINT('Origin',(0.,6.5,14.5));
#30571=CARTESIAN_POINT('Origin',(0.,6.5,12.8));
#30572=CARTESIAN_POINT('Origin',(-1.5,5.,12.8));
#30573=CARTESIAN_POINT('',(-1.665,5.,12.8));
#30574=CARTESIAN_POINT('Origin',(-1.5,5.,12.8));
#30575=CARTESIAN_POINT('',(-1.665,5.,14.5));
#30576=CARTESIAN_POINT('',(-1.665,5.,12.8));
#30577=CARTESIAN_POINT('Origin',(-1.5,5.,14.5));
#30578=CARTESIAN_POINT('Origin',(-1.5,5.,12.8));
#30579=CARTESIAN_POINT('Origin',(0.,5.,12.5));
#30580=CARTESIAN_POINT('',(-1.11,5.,14.5));
#30581=CARTESIAN_POINT('Origin',(0.,5.,14.5));
#30582=CARTESIAN_POINT('',(-1.11,5.,12.5));
#30583=CARTESIAN_POINT('',(-1.11,5.,12.5));
#30584=CARTESIAN_POINT('Origin',(0.,5.,12.5));
#30585=CARTESIAN_POINT('Origin',(0.,5.,12.5));
#30586=CARTESIAN_POINT('',(-2.2,5.,14.5));
#30587=CARTESIAN_POINT('Origin',(0.,5.,14.5));
#30588=CARTESIAN_POINT('',(-2.2,5.,12.5));
#30589=CARTESIAN_POINT('',(-2.2,5.,12.5));
#30590=CARTESIAN_POINT('Origin',(0.,5.,12.5));
#30591=CARTESIAN_POINT('Origin',(0.,5.,14.5));
#30592=CARTESIAN_POINT('Origin',(0.,5.,12.5));
#43433=UNCERTAINTY_MEASURE_WITH_UNIT(LENGTH_MEASURE(0.001),#43522,
'DISTANCE_ACCURACY_VALUE',
'Maximum model space distance between geometric entities at asserted c
onnectivities');
#43453=UNCERTAINTY_MEASURE_WITH_UNIT(LENGTH_MEASURE(0.001),#43522,
'DISTANCE_ACCURACY_VALUE',
'Maximum model space distance between geometric entities at asserted c
onnectivities');
#43501=(
GEOMETRIC_REPRESENTATION_CONTEXT(3)
GLOBAL_UNCERTAINTY_ASSIGNED_CONTEXT((#43433))
GLOBAL_UNIT_ASSIGNED_CONTEXT((#43522,#43524,#43525))
REPRESENTATION_CONTEXT('','3D')
);
#43521=(
GEOMETRIC_REPRESENTATION_CONTEXT(3)
GLOBAL_UNCERTAINTY_ASSIGNED_CONTEXT((#43453))
GLOBAL_UNIT_ASSIGNED_CONTEXT((#43522,#43524,#43525))
REPRESENTATION_CONTEXT('','3D')
);
#43522=(
LENGTH_UNIT()
NAMED_UNIT(*)
SI_UNIT(.CENTI.,.METRE.)
);
#43524=(
NAMED_UNIT(*)
PLANE_ANGLE_UNIT()
SI_UNIT($,.RADIAN.)
);
#43525=(
NAMED_UNIT(*)
SI_UNIT($,.STERADIAN.)
SOLID_ANGLE_UNIT()
);
#43573=SHAPE_DEFINITION_REPRESENTATION(#43650,#43841);
#43650=PRODUCT_DEFINITION_SHAPE('',$,#43909);
#43841=SHAPE_REPRESENTATION('',(#20586),#43501);
#43861=PRODUCT_DEFINITION_CONTEXT('part definition',#44064,'design');
#43909=PRODUCT_DEFINITION('Nut carrier','Nut carrier',#43976,#43861);
#43976=PRODUCT_DEFINITION_FORMATION('',$,#44113);
#44064=APPLICATION_CONTEXT(
'Core Data for Automotive Mechanical Design Process');
#44065=PRODUCT_CONTEXT('part definition',#44064,'mechanical');
#44113=PRODUCT('Nut carrier','Nut carrier','Nut carrier',(#44065));
#44203=COLOUR_RGB('Black',0.12,0.14,0.17);
#44204=FILL_AREA_STYLE_COLOUR('',#44203);
#44205=FILL_AREA_STYLE('',(#44204));
#44206=SURFACE_STYLE_FILL_AREA(#44205);
#44207=SURFACE_SIDE_STYLE('',(#44206));
#44208=SURFACE_STYLE_USAGE(.BOTH.,#44207);
#44209=PRESENTATION_STYLE_ASSIGNMENT((#44208));
ENDSEC;
END-ISO-10303-21;
